ISO-10303-21;
HEADER;
/* Generated by software containing ST-Developer
 * from STEP Tools, Inc. (www.steptools.com) 
 */

FILE_DESCRIPTION(
/* description */ ('Independent manual traversing gantry with native reusable aluminum pr
ofiles,180mm captured carriage travel, four bronze-bushed rollers, lin
ked ideal rolling motion, bonded acetal lateral guides, positive welde
d end stops and fully retained axle stacks. Editable native profile cu
t lengths220/400mm. Tool attachments viaM6 bridge-plate taps; mounted 
tool outside assembly. Welds, anchors, adhesives, fits, traction, load
/speed/structural/life ratings unassigned.'),
/* implementation_level */ '2;1');

FILE_NAME(
/* name */ 'Axle thrust washer.step',
/* time_stamp */ '2026-11-09T20:04:38-08:00',
/* author */ (''),
/* organization */ (''),
/* preprocessor_version */ 'ST-DEVELOPER v20.2',
/* originating_system */ 'Autodesk Translation Framework v15.17.0.0',
/* authorisation */ '');

FILE_SCHEMA (('AUTOMOTIVE_DESIGN { 1 0 10303 214 3 1 1 }'));
ENDSEC;

DATA;
#10=MECHANICAL_DESIGN_GEOMETRIC_PRESENTATION_REPRESENTATION('',(#486),#13231);
#454=SHAPE_REPRESENTATION_RELATIONSHIP('SRR','None',#13343,#470);
#470=ADVANCED_BREP_SHAPE_REPRESENTATION('',(#502),#13230);
#486=STYLED_ITEM('',(#13421),#502);
#502=MANIFOLD_SOLID_BREP('Body1',#4166);
#550=FACE_BOUND('',#1121,.T.);
#551=FACE_BOUND('',#1123,.T.);
#631=PLANE('',#4676);
#632=PLANE('',#4677);
#850=FACE_OUTER_BOUND('',#1118,.T.);
#851=FACE_OUTER_BOUND('',#1119,.T.);
#852=FACE_OUTER_BOUND('',#1120,.T.);
#853=FACE_OUTER_BOUND('',#1122,.T.);
#1118=EDGE_LOOP('',(#3786,#3787,#3788,#3789));
#1119=EDGE_LOOP('',(#3790,#3791,#3792,#3793));
#1120=EDGE_LOOP('',(#3794));
#1121=EDGE_LOOP('',(#3795));
#1122=EDGE_LOOP('',(#3796));
#1123=EDGE_LOOP('',(#3797));
#1384=LINE('',#13129,#1646);
#1385=LINE('',#13135,#1647);
#1646=VECTOR('',#5651,6.);
#1647=VECTOR('',#5658,11.);
#1748=CIRCLE('',#4671,6.);
#1749=CIRCLE('',#4672,6.);
#1750=CIRCLE('',#4674,11.);
#1751=CIRCLE('',#4675,11.);
#2120=VERTEX_POINT('',#13126);
#2121=VERTEX_POINT('',#13128);
#2122=VERTEX_POINT('',#13132);
#2123=VERTEX_POINT('',#13134);
#2676=EDGE_CURVE('',#2120,#2120,#1748,.T.);
#2677=EDGE_CURVE('',#2120,#2121,#1384,.T.);
#2678=EDGE_CURVE('',#2121,#2121,#1749,.T.);
#2679=EDGE_CURVE('',#2122,#2122,#1750,.T.);
#2680=EDGE_CURVE('',#2122,#2123,#1385,.T.);
#2681=EDGE_CURVE('',#2123,#2123,#1751,.T.);
#3786=ORIENTED_EDGE('',*,*,#2676,.F.);
#3787=ORIENTED_EDGE('',*,*,#2677,.T.);
#3788=ORIENTED_EDGE('',*,*,#2678,.T.);
#3789=ORIENTED_EDGE('',*,*,#2677,.F.);
#3790=ORIENTED_EDGE('',*,*,#2679,.F.);
#3791=ORIENTED_EDGE('',*,*,#2680,.T.);
#3792=ORIENTED_EDGE('',*,*,#2681,.T.);
#3793=ORIENTED_EDGE('',*,*,#2680,.F.);
#3794=ORIENTED_EDGE('',*,*,#2679,.T.);
#3795=ORIENTED_EDGE('',*,*,#2676,.T.);
#3796=ORIENTED_EDGE('',*,*,#2681,.F.);
#3797=ORIENTED_EDGE('',*,*,#2678,.F.);
#3928=CYLINDRICAL_SURFACE('',#4670,6.);
#3929=CYLINDRICAL_SURFACE('',#4673,11.);
#4147=ADVANCED_FACE('',(#850),#3928,.F.);
#4148=ADVANCED_FACE('',(#851),#3929,.T.);
#4149=ADVANCED_FACE('',(#852,#550),#631,.T.);
#4150=ADVANCED_FACE('',(#853,#551),#632,.F.);
#4166=CLOSED_SHELL('',(#4147,#4148,#4149,#4150));
#4669=AXIS2_PLACEMENT_3D('',#13124,#5645,#5646);
#4670=AXIS2_PLACEMENT_3D('',#13125,#5647,#5648);
#4671=AXIS2_PLACEMENT_3D('',#13127,#5649,#5650);
#4672=AXIS2_PLACEMENT_3D('',#13130,#5652,#5653);
#4673=AXIS2_PLACEMENT_3D('',#13131,#5654,#5655);
#4674=AXIS2_PLACEMENT_3D('',#13133,#5656,#5657);
#4675=AXIS2_PLACEMENT_3D('',#13136,#5659,#5660);
#4676=AXIS2_PLACEMENT_3D('',#13137,#5661,#5662);
#4677=AXIS2_PLACEMENT_3D('',#13138,#5663,#5664);
#5645=DIRECTION('axis',(0.,0.,1.));
#5646=DIRECTION('refdir',(1.,0.,0.));
#5647=DIRECTION('center_axis',(0.,0.,1.));
#5648=DIRECTION('ref_axis',(1.,0.,0.));
#5649=DIRECTION('center_axis',(0.,0.,-1.));
#5650=DIRECTION('ref_axis',(1.,0.,0.));
#5651=DIRECTION('',(0.,0.,-1.));
#5652=DIRECTION('center_axis',(0.,0.,-1.));
#5653=DIRECTION('ref_axis',(1.,0.,0.));
#5654=DIRECTION('center_axis',(0.,0.,1.));
#5655=DIRECTION('ref_axis',(1.,0.,0.));
#5656=DIRECTION('center_axis',(0.,0.,1.));
#5657=DIRECTION('ref_axis',(1.,0.,0.));
#5658=DIRECTION('',(0.,0.,-1.));
#5659=DIRECTION('center_axis',(0.,0.,1.));
#5660=DIRECTION('ref_axis',(1.,0.,0.));
#5661=DIRECTION('center_axis',(0.,0.,1.));
#5662=DIRECTION('ref_axis',(1.,0.,0.));
#5663=DIRECTION('center_axis',(0.,0.,1.));
#5664=DIRECTION('ref_axis',(1.,0.,0.));
#13124=CARTESIAN_POINT('',(0.,0.,0.));
#13125=CARTESIAN_POINT('Origin',(0.,0.,0.));
#13126=CARTESIAN_POINT('',(-6.,-7.34788079488412E-16,2.));
#13127=CARTESIAN_POINT('Origin',(0.,0.,2.));
#13128=CARTESIAN_POINT('',(-6.,-7.34788079488412E-16,0.));
#13129=CARTESIAN_POINT('',(-6.,-7.34788079488412E-16,0.));
#13130=CARTESIAN_POINT('Origin',(0.,0.,0.));
#13131=CARTESIAN_POINT('Origin',(0.,0.,0.));
#13132=CARTESIAN_POINT('',(-11.,-1.34711147906209E-15,2.));
#13133=CARTESIAN_POINT('Origin',(0.,0.,2.));
#13134=CARTESIAN_POINT('',(-11.,-1.34711147906209E-15,0.));
#13135=CARTESIAN_POINT('',(-11.,-1.34711147906209E-15,0.));
#13136=CARTESIAN_POINT('Origin',(0.,0.,0.));
#13137=CARTESIAN_POINT('Origin',(0.,0.,2.));
#13138=CARTESIAN_POINT('Origin',(0.,0.,0.));
#13212=UNCERTAINTY_MEASURE_WITH_UNIT(LENGTH_MEASURE(0.01),#13232,
'DISTANCE_ACCURACY_VALUE',
'Maximum model space distance between geometric entities at asserted c
onnectivities');
#13213=UNCERTAINTY_MEASURE_WITH_UNIT(LENGTH_MEASURE(0.01),#13232,
'DISTANCE_ACCURACY_VALUE',
'Maximum model space distance between geometric entities at asserted c
onnectivities');
#13230=(
GEOMETRIC_REPRESENTATION_CONTEXT(3)
GLOBAL_UNCERTAINTY_ASSIGNED_CONTEXT((#13212))
GLOBAL_UNIT_ASSIGNED_CONTEXT((#13232,#13234,#13235))
REPRESENTATION_CONTEXT('','3D')
);
#13231=(
GEOMETRIC_REPRESENTATION_CONTEXT(3)
GLOBAL_UNCERTAINTY_ASSIGNED_CONTEXT((#13213))
GLOBAL_UNIT_ASSIGNED_CONTEXT((#13232,#13234,#13235))
REPRESENTATION_CONTEXT('','3D')
);
#13232=(
LENGTH_UNIT()
NAMED_UNIT(*)
SI_UNIT(.MILLI.,.METRE.)
);
#13234=(
NAMED_UNIT(*)
PLANE_ANGLE_UNIT()
SI_UNIT($,.RADIAN.)
);
#13235=(
NAMED_UNIT(*)
SI_UNIT($,.STERADIAN.)
SOLID_ANGLE_UNIT()
);
#13252=SHAPE_DEFINITION_REPRESENTATION(#13269,#13343);
#13269=PRODUCT_DEFINITION_SHAPE('',$,#13361);
#13343=SHAPE_REPRESENTATION('',(#4669),#13230);
#13344=PRODUCT_DEFINITION_CONTEXT('part definition',#13397,'design');
#13361=PRODUCT_DEFINITION('Axle thrust washer','Axle thrust washer',#13378,
#13344);
#13378=PRODUCT_DEFINITION_FORMATION('',$,#13415);
#13397=APPLICATION_CONTEXT(
'Core Data for Automotive Mechanical Design Process');
#13398=PRODUCT_CONTEXT('part definition',#13397,'mechanical');
#13415=PRODUCT('Axle thrust washer','Axle thrust washer',$,(#13398));
#13421=PRESENTATION_STYLE_ASSIGNMENT((#13435));
#13435=SURFACE_STYLE_USAGE(.BOTH.,#13449);
#13449=SURFACE_SIDE_STYLE('',(#13463));
#13463=SURFACE_STYLE_FILL_AREA(#13477);
#13477=FILL_AREA_STYLE('Light gray',(#13491));
#13491=FILL_AREA_STYLE_COLOUR('Light gray',#13505);
#13505=COLOUR_RGB('Light gray',0.725490196078431,0.752941176470588,0.792156862745098);
ENDSEC;
END-ISO-10303-21;
